ISO-10303-21;
HEADER;
/* Generated by software containing ST-Developer
 * from STEP Tools, Inc. (www.steptools.com) 
 */

FILE_DESCRIPTION(
/* description */ ('Turntable on roller ring'),
/* implementation_level */ '2;1');

FILE_NAME(
/* name */ 'Outer race retainer (6).step',
/* time_stamp */ '2026-10-28T03:23:59-07:00',
/* author */ (''),
/* organization */ (''),
/* preprocessor_version */ 'ST-DEVELOPER v20.2',
/* originating_system */ 'Autodesk Translation Framework v15.17.0.0',
/* authorisation */ '');

FILE_SCHEMA (('AUTOMOTIVE_DESIGN { 1 0 10303 214 3 1 1 }'));
ENDSEC;

DATA;
#10=MECHANICAL_DESIGN_GEOMETRIC_PRESENTATION_REPRESENTATION('',(#674),#16281);
#555=SHAPE_REPRESENTATION_RELATIONSHIP('SRR','None',#16579,#610);
#610=ADVANCED_BREP_SHAPE_REPRESENTATION('',(#742),#16273);
#674=STYLED_ITEM('',(#16932),#742);
#742=MANIFOLD_SOLID_BREP('Body1',#8419);
#977=FACE_BOUND('',#2424,.T.);
#978=FACE_BOUND('',#2426,.T.);
#1229=PLANE('',#10029);
#1230=PLANE('',#10030);
#1696=FACE_OUTER_BOUND('',#2421,.T.);
#1697=FACE_OUTER_BOUND('',#2422,.T.);
#1698=FACE_OUTER_BOUND('',#2423,.T.);
#1699=FACE_OUTER_BOUND('',#2425,.T.);
#2421=EDGE_LOOP('',(#7433,#7434,#7435,#7436));
#2422=EDGE_LOOP('',(#7437,#7438,#7439,#7440));
#2423=EDGE_LOOP('',(#7441));
#2424=EDGE_LOOP('',(#7442));
#2425=EDGE_LOOP('',(#7443));
#2426=EDGE_LOOP('',(#7444));
#2956=LINE('',#15507,#3439);
#2957=LINE('',#15513,#3440);
#3439=VECTOR('',#12633,1.1);
#3440=VECTOR('',#12640,1.5);
#3869=CIRCLE('',#10024,1.1);
#3870=CIRCLE('',#10025,1.1);
#3871=CIRCLE('',#10027,1.5);
#3872=CIRCLE('',#10028,1.5);
#4545=VERTEX_POINT('',#15504);
#4546=VERTEX_POINT('',#15506);
#4547=VERTEX_POINT('',#15510);
#4548=VERTEX_POINT('',#15512);
#5527=EDGE_CURVE('',#4545,#4545,#3869,.T.);
#5528=EDGE_CURVE('',#4545,#4546,#2956,.T.);
#5529=EDGE_CURVE('',#4546,#4546,#3870,.T.);
#5530=EDGE_CURVE('',#4547,#4547,#3871,.T.);
#5531=EDGE_CURVE('',#4547,#4548,#2957,.T.);
#5532=EDGE_CURVE('',#4548,#4548,#3872,.T.);
#7433=ORIENTED_EDGE('',*,*,#5527,.F.);
#7434=ORIENTED_EDGE('',*,*,#5528,.T.);
#7435=ORIENTED_EDGE('',*,*,#5529,.T.);
#7436=ORIENTED_EDGE('',*,*,#5528,.F.);
#7437=ORIENTED_EDGE('',*,*,#5530,.F.);
#7438=ORIENTED_EDGE('',*,*,#5531,.T.);
#7439=ORIENTED_EDGE('',*,*,#5532,.T.);
#7440=ORIENTED_EDGE('',*,*,#5531,.F.);
#7441=ORIENTED_EDGE('',*,*,#5530,.T.);
#7442=ORIENTED_EDGE('',*,*,#5527,.T.);
#7443=ORIENTED_EDGE('',*,*,#5532,.F.);
#7444=ORIENTED_EDGE('',*,*,#5529,.F.);
#7837=CYLINDRICAL_SURFACE('',#10023,1.1);
#7838=CYLINDRICAL_SURFACE('',#10026,1.5);
#8299=ADVANCED_FACE('',(#1696),#7837,.F.);
#8300=ADVANCED_FACE('',(#1697),#7838,.T.);
#8301=ADVANCED_FACE('',(#1698,#977),#1229,.T.);
#8302=ADVANCED_FACE('',(#1699,#978),#1230,.F.);
#8419=CLOSED_SHELL('',(#8299,#8300,#8301,#8302));
#10022=AXIS2_PLACEMENT_3D('',#15502,#12627,#12628);
#10023=AXIS2_PLACEMENT_3D('',#15503,#12629,#12630);
#10024=AXIS2_PLACEMENT_3D('',#15505,#12631,#12632);
#10025=AXIS2_PLACEMENT_3D('',#15508,#12634,#12635);
#10026=AXIS2_PLACEMENT_3D('',#15509,#12636,#12637);
#10027=AXIS2_PLACEMENT_3D('',#15511,#12638,#12639);
#10028=AXIS2_PLACEMENT_3D('',#15514,#12641,#12642);
#10029=AXIS2_PLACEMENT_3D('',#15515,#12643,#12644);
#10030=AXIS2_PLACEMENT_3D('',#15516,#12645,#12646);
#12627=DIRECTION('axis',(0.,0.,1.));
#12628=DIRECTION('refdir',(1.,0.,0.));
#12629=DIRECTION('center_axis',(0.,1.,0.));
#12630=DIRECTION('ref_axis',(1.,0.,0.));
#12631=DIRECTION('center_axis',(0.,-1.,0.));
#12632=DIRECTION('ref_axis',(1.,0.,0.));
#12633=DIRECTION('',(0.,-1.,0.));
#12634=DIRECTION('center_axis',(0.,-1.,0.));
#12635=DIRECTION('ref_axis',(1.,0.,0.));
#12636=DIRECTION('center_axis',(0.,1.,0.));
#12637=DIRECTION('ref_axis',(1.,0.,0.));
#12638=DIRECTION('center_axis',(0.,1.,0.));
#12639=DIRECTION('ref_axis',(1.,0.,0.));
#12640=DIRECTION('',(0.,-1.,0.));
#12641=DIRECTION('center_axis',(0.,1.,0.));
#12642=DIRECTION('ref_axis',(1.,0.,0.));
#12643=DIRECTION('center_axis',(0.,1.,0.));
#12644=DIRECTION('ref_axis',(1.,0.,0.));
#12645=DIRECTION('center_axis',(0.,1.,0.));
#12646=DIRECTION('ref_axis',(1.,0.,0.));
#15502=CARTESIAN_POINT('',(0.,0.,0.));
#15503=CARTESIAN_POINT('Origin',(0.,14.35,3.5));
#15504=CARTESIAN_POINT('',(-1.1,14.55,3.5));
#15505=CARTESIAN_POINT('Origin',(0.,14.55,3.5));
#15506=CARTESIAN_POINT('',(-1.1,14.35,3.5));
#15507=CARTESIAN_POINT('',(-1.1,14.35,3.5));
#15508=CARTESIAN_POINT('Origin',(0.,14.35,3.5));
#15509=CARTESIAN_POINT('Origin',(0.,14.35,3.5));
#15510=CARTESIAN_POINT('',(-1.5,14.55,3.5));
#15511=CARTESIAN_POINT('Origin',(0.,14.55,3.5));
#15512=CARTESIAN_POINT('',(-1.5,14.35,3.5));
#15513=CARTESIAN_POINT('',(-1.5,14.35,3.5));
#15514=CARTESIAN_POINT('Origin',(0.,14.35,3.5));
#15515=CARTESIAN_POINT('Origin',(0.,14.55,3.5));
#15516=CARTESIAN_POINT('Origin',(0.,14.35,3.5));
#16204=UNCERTAINTY_MEASURE_WITH_UNIT(LENGTH_MEASURE(0.001),#16282,
'DISTANCE_ACCURACY_VALUE',
'Maximum model space distance between geometric entities at asserted c
onnectivities');
#16212=UNCERTAINTY_MEASURE_WITH_UNIT(LENGTH_MEASURE(0.001),#16282,
'DISTANCE_ACCURACY_VALUE',
'Maximum model space distance between geometric entities at asserted c
onnectivities');
#16273=(
GEOMETRIC_REPRESENTATION_CONTEXT(3)
GLOBAL_UNCERTAINTY_ASSIGNED_CONTEXT((#16204))
GLOBAL_UNIT_ASSIGNED_CONTEXT((#16282,#16284,#16285))
REPRESENTATION_CONTEXT('','3D')
);
#16281=(
GEOMETRIC_REPRESENTATION_CONTEXT(3)
GLOBAL_UNCERTAINTY_ASSIGNED_CONTEXT((#16212))
GLOBAL_UNIT_ASSIGNED_CONTEXT((#16282,#16284,#16285))
REPRESENTATION_CONTEXT('','3D')
);
#16282=(
LENGTH_UNIT()
NAMED_UNIT(*)
SI_UNIT(.CENTI.,.METRE.)
);
#16284=(
NAMED_UNIT(*)
PLANE_ANGLE_UNIT()
SI_UNIT($,.RADIAN.)
);
#16285=(
NAMED_UNIT(*)
SI_UNIT($,.STERADIAN.)
SOLID_ANGLE_UNIT()
);
#16346=SHAPE_DEFINITION_REPRESENTATION(#16480,#16579);
#16480=PRODUCT_DEFINITION_SHAPE('',$,#16648);
#16579=SHAPE_REPRESENTATION('',(#10022),#16273);
#16587=PRODUCT_DEFINITION_CONTEXT('part definition',#16793,'design');
#16648=PRODUCT_DEFINITION('Outer race retainer (6)',
'Outer race retainer (6)',#16716,#16587);
#16716=PRODUCT_DEFINITION_FORMATION('',$,#16855);
#16793=APPLICATION_CONTEXT(
'Core Data for Automotive Mechanical Design Process');
#16794=PRODUCT_CONTEXT('part definition',#16793,'mechanical');
#16855=PRODUCT('Outer race retainer (6)','Outer race retainer (6)',
'Outer race retainer (6)',(#16794));
#16926=COLOUR_RGB('Grey',0.48,0.52,0.57);
#16927=FILL_AREA_STYLE_COLOUR('',#16926);
#16928=FILL_AREA_STYLE('',(#16927));
#16929=SURFACE_STYLE_FILL_AREA(#16928);
#16930=SURFACE_SIDE_STYLE('',(#16929));
#16931=SURFACE_STYLE_USAGE(.BOTH.,#16930);
#16932=PRESENTATION_STYLE_ASSIGNMENT((#16931));
ENDSEC;
END-ISO-10303-21;
